ISO-10303-21;
HEADER;
/* Generated by software containing ST-Developer
 * from STEP Tools, Inc. (www.steptools.com) 
 */

FILE_DESCRIPTION(
/* description */ ('V-block with clamp strap'),
/* implementation_level */ '2;1');

FILE_NAME(
/* name */ 'Hex Nut - M8.step',
/* time_stamp */ '2026-10-27T10:50:53-07:00',
/* author */ (''),
/* organization */ (''),
/* preprocessor_version */ 'ST-DEVELOPER v20.2',
/* originating_system */ 'Autodesk Translation Framework v15.17.0.0',
/* authorisation */ '');

FILE_SCHEMA (('AUTOMOTIVE_DESIGN { 1 0 10303 214 3 1 1 }'));
ENDSEC;

DATA;
#10=MECHANICAL_DESIGN_GEOMETRIC_PRESENTATION_REPRESENTATION('',(#285),#7344);
#187=(
BOUNDED_CURVE()
B_SPLINE_CURVE(2,(#7192,#7193,#7194),.UNSPECIFIED.,.F.,.F.)
B_SPLINE_CURVE_WITH_KNOTS((3,3),(0.14973948338295,0.97160236658079),
 .UNSPECIFIED.)
CURVE()
GEOMETRIC_REPRESENTATION_ITEM()
RATIONAL_B_SPLINE_CURVE((1.07140024848292,1.23714644374248,1.07140024848292))
REPRESENTATION_ITEM('')
);
#188=(
BOUNDED_CURVE()
B_SPLINE_CURVE(2,(#7196,#7197,#7198),.UNSPECIFIED.,.F.,.F.)
B_SPLINE_CURVE_WITH_KNOTS((3,3),(0.14973948338295,0.971602366580789),
 .UNSPECIFIED.)
CURVE()
GEOMETRIC_REPRESENTATION_ITEM()
RATIONAL_B_SPLINE_CURVE((1.07140024848292,1.23714644374248,1.07140024848292))
REPRESENTATION_ITEM('')
);
#189=(
BOUNDED_CURVE()
B_SPLINE_CURVE(2,(#7203,#7204,#7205),.UNSPECIFIED.,.F.,.F.)
B_SPLINE_CURVE_WITH_KNOTS((3,3),(0.14973948338295,0.97160236658079),
 .UNSPECIFIED.)
CURVE()
GEOMETRIC_REPRESENTATION_ITEM()
RATIONAL_B_SPLINE_CURVE((1.07140024848292,1.23714644374248,1.07140024848292))
REPRESENTATION_ITEM('')
);
#190=(
BOUNDED_CURVE()
B_SPLINE_CURVE(2,(#7207,#7208,#7209),.UNSPECIFIED.,.F.,.F.)
B_SPLINE_CURVE_WITH_KNOTS((3,3),(0.14973948338295,0.97160236658079),
 .UNSPECIFIED.)
CURVE()
GEOMETRIC_REPRESENTATION_ITEM()
RATIONAL_B_SPLINE_CURVE((1.07140024848292,1.23714644374248,1.07140024848292))
REPRESENTATION_ITEM('')
);
#191=(
BOUNDED_CURVE()
B_SPLINE_CURVE(2,(#7211,#7212,#7213),.UNSPECIFIED.,.F.,.F.)
B_SPLINE_CURVE_WITH_KNOTS((3,3),(0.14973948338295,0.971602366580789),
 .UNSPECIFIED.)
CURVE()
GEOMETRIC_REPRESENTATION_ITEM()
RATIONAL_B_SPLINE_CURVE((1.07140024848292,1.23714644374248,1.07140024848292))
REPRESENTATION_ITEM('')
);
#192=(
BOUNDED_CURVE()
B_SPLINE_CURVE(2,(#7214,#7215,#7216),.UNSPECIFIED.,.F.,.F.)
B_SPLINE_CURVE_WITH_KNOTS((3,3),(0.14973948338295,0.97160236658079),
 .UNSPECIFIED.)
CURVE()
GEOMETRIC_REPRESENTATION_ITEM()
RATIONAL_B_SPLINE_CURVE((1.07140024848292,1.23714644374248,1.07140024848292))
REPRESENTATION_ITEM('')
);
#193=(
BOUNDED_CURVE()
B_SPLINE_CURVE(2,(#7223,#7224,#7225),.UNSPECIFIED.,.F.,.F.)
B_SPLINE_CURVE_WITH_KNOTS((3,3),(0.14973948338295,0.97160236658079),
 .UNSPECIFIED.)
CURVE()
GEOMETRIC_REPRESENTATION_ITEM()
RATIONAL_B_SPLINE_CURVE((1.07140024848292,1.23714644374248,1.07140024848292))
REPRESENTATION_ITEM('')
);
#194=(
BOUNDED_CURVE()
B_SPLINE_CURVE(2,(#7227,#7228,#7229),.UNSPECIFIED.,.F.,.F.)
B_SPLINE_CURVE_WITH_KNOTS((3,3),(0.14973948338295,0.97160236658079),
 .UNSPECIFIED.)
CURVE()
GEOMETRIC_REPRESENTATION_ITEM()
RATIONAL_B_SPLINE_CURVE((1.07140024848292,1.23714644374248,1.07140024848292))
REPRESENTATION_ITEM('')
);
#195=(
BOUNDED_CURVE()
B_SPLINE_CURVE(2,(#7231,#7232,#7233),.UNSPECIFIED.,.F.,.F.)
B_SPLINE_CURVE_WITH_KNOTS((3,3),(0.14973948338295,0.971602366580789),
 .UNSPECIFIED.)
CURVE()
GEOMETRIC_REPRESENTATION_ITEM()
RATIONAL_B_SPLINE_CURVE((1.07140024848292,1.23714644374248,1.07140024848292))
REPRESENTATION_ITEM('')
);
#196=(
BOUNDED_CURVE()
B_SPLINE_CURVE(2,(#7235,#7236,#7237),.UNSPECIFIED.,.F.,.F.)
B_SPLINE_CURVE_WITH_KNOTS((3,3),(0.14973948338295,0.97160236658079),
 .UNSPECIFIED.)
CURVE()
GEOMETRIC_REPRESENTATION_ITEM()
RATIONAL_B_SPLINE_CURVE((1.07140024848292,1.23714644374248,1.07140024848292))
REPRESENTATION_ITEM('')
);
#197=(
BOUNDED_CURVE()
B_SPLINE_CURVE(2,(#7239,#7240,#7241),.UNSPECIFIED.,.F.,.F.)
B_SPLINE_CURVE_WITH_KNOTS((3,3),(0.14973948338295,0.97160236658079),
 .UNSPECIFIED.)
CURVE()
GEOMETRIC_REPRESENTATION_ITEM()
RATIONAL_B_SPLINE_CURVE((1.07140024848292,1.23714644374248,1.07140024848292))
REPRESENTATION_ITEM('')
);
#198=(
BOUNDED_CURVE()
B_SPLINE_CURVE(2,(#7242,#7243,#7244),.UNSPECIFIED.,.F.,.F.)
B_SPLINE_CURVE_WITH_KNOTS((3,3),(0.14973948338295,0.971602366580789),
 .UNSPECIFIED.)
CURVE()
GEOMETRIC_REPRESENTATION_ITEM()
RATIONAL_B_SPLINE_CURVE((1.07140024848292,1.23714644374248,1.07140024848292))
REPRESENTATION_ITEM('')
);
#215=CONICAL_SURFACE('',#4803,0.734027674973257,1.0471975511966);
#216=CONICAL_SURFACE('',#4805,0.734027674973257,1.0471975511966);
#243=SHAPE_REPRESENTATION_RELATIONSHIP('SRR','None',#7462,#264);
#264=ADVANCED_BREP_SHAPE_REPRESENTATION('',(#303),#7341);
#285=STYLED_ITEM('',(#7638),#303);
#303=MANIFOLD_SOLID_BREP('Body1',#4170);
#374=FACE_BOUND('',#1107,.T.);
#375=FACE_BOUND('',#1109,.T.);
#499=CIRCLE('',#4804,0.6175);
#500=CIRCLE('',#4806,0.6175);
#501=CIRCLE('',#4811,0.338975);
#502=CIRCLE('',#4812,0.338975);
#560=CYLINDRICAL_SURFACE('',#4810,0.338975);
#788=FACE_OUTER_BOUND('',#1097,.T.);
#789=FACE_OUTER_BOUND('',#1098,.T.);
#790=FACE_OUTER_BOUND('',#1099,.T.);
#791=FACE_OUTER_BOUND('',#1100,.T.);
#792=FACE_OUTER_BOUND('',#1101,.T.);
#793=FACE_OUTER_BOUND('',#1102,.T.);
#794=FACE_OUTER_BOUND('',#1103,.T.);
#795=FACE_OUTER_BOUND('',#1104,.T.);
#796=FACE_OUTER_BOUND('',#1105,.T.);
#797=FACE_OUTER_BOUND('',#1106,.T.);
#798=FACE_OUTER_BOUND('',#1108,.T.);
#1097=EDGE_LOOP('',(#3684,#3685,#3686,#3687,#3688,#3689,#3690,#3691,#3692));
#1098=EDGE_LOOP('',(#3693,#3694,#3695,#3696,#3697,#3698,#3699,#3700,#3701));
#1099=EDGE_LOOP('',(#3702,#3703,#3704,#3705));
#1100=EDGE_LOOP('',(#3706,#3707,#3708,#3709));
#1101=EDGE_LOOP('',(#3710,#3711,#3712,#3713));
#1102=EDGE_LOOP('',(#3714,#3715,#3716,#3717));
#1103=EDGE_LOOP('',(#3718,#3719,#3720,#3721));
#1104=EDGE_LOOP('',(#3722,#3723,#3724,#3725));
#1105=EDGE_LOOP('',(#3726,#3727,#3728,#3729));
#1106=EDGE_LOOP('',(#3730));
#1107=EDGE_LOOP('',(#3731));
#1108=EDGE_LOOP('',(#3732));
#1109=EDGE_LOOP('',(#3733));
#1468=LINE('',#7200,#1833);
#1469=LINE('',#7221,#1834);
#1470=LINE('',#7246,#1835);
#1471=LINE('',#7247,#1836);
#1472=LINE('',#7249,#1837);
#1473=LINE('',#7251,#1838);
#1474=LINE('',#7256,#1839);
#1475=LINE('',#7259,#1840);
#1476=LINE('',#7261,#1841);
#1833=VECTOR('',#5998,0.734027674973257);
#1834=VECTOR('',#6005,0.734027674973257);
#1835=VECTOR('',#6008,1.);
#1836=VECTOR('',#6009,1.);
#1837=VECTOR('',#6012,1.);
#1838=VECTOR('',#6015,1.);
#1839=VECTOR('',#6020,0.4);
#1840=VECTOR('',#6025,1.);
#1841=VECTOR('',#6028,1.);
#2156=VERTEX_POINT('',#7190);
#2157=VERTEX_POINT('',#7191);
#2158=VERTEX_POINT('',#7195);
#2159=VERTEX_POINT('',#7199);
#2160=VERTEX_POINT('',#7202);
#2161=VERTEX_POINT('',#7206);
#2162=VERTEX_POINT('',#7210);
#2163=VERTEX_POINT('',#7218);
#2164=VERTEX_POINT('',#7220);
#2165=VERTEX_POINT('',#7222);
#2166=VERTEX_POINT('',#7226);
#2167=VERTEX_POINT('',#7230);
#2168=VERTEX_POINT('',#7234);
#2169=VERTEX_POINT('',#7238);
#2170=VERTEX_POINT('',#7253);
#2171=VERTEX_POINT('',#7255);
#2668=EDGE_CURVE('',#2156,#2157,#187,.T.);
#2669=EDGE_CURVE('',#2158,#2156,#188,.T.);
#2670=EDGE_CURVE('',#2158,#2159,#1468,.T.);
#2671=EDGE_CURVE('',#2159,#2159,#499,.T.);
#2672=EDGE_CURVE('',#2160,#2158,#189,.T.);
#2673=EDGE_CURVE('',#2161,#2160,#190,.T.);
#2674=EDGE_CURVE('',#2162,#2161,#191,.T.);
#2675=EDGE_CURVE('',#2157,#2162,#192,.T.);
#2676=EDGE_CURVE('',#2163,#2163,#500,.T.);
#2677=EDGE_CURVE('',#2163,#2164,#1469,.T.);
#2678=EDGE_CURVE('',#2165,#2164,#193,.T.);
#2679=EDGE_CURVE('',#2166,#2165,#194,.T.);
#2680=EDGE_CURVE('',#2167,#2166,#195,.T.);
#2681=EDGE_CURVE('',#2168,#2167,#196,.T.);
#2682=EDGE_CURVE('',#2169,#2168,#197,.T.);
#2683=EDGE_CURVE('',#2164,#2169,#198,.T.);
#2684=EDGE_CURVE('',#2160,#2169,#1470,.T.);
#2685=EDGE_CURVE('',#2161,#2168,#1471,.T.);
#2686=EDGE_CURVE('',#2158,#2164,#1472,.T.);
#2687=EDGE_CURVE('',#2156,#2165,#1473,.T.);
#2688=EDGE_CURVE('',#2170,#2170,#501,.F.);
#2689=EDGE_CURVE('',#2170,#2171,#1474,.T.);
#2690=EDGE_CURVE('',#2171,#2171,#502,.F.);
#2691=EDGE_CURVE('',#2157,#2166,#1475,.T.);
#2692=EDGE_CURVE('',#2162,#2167,#1476,.T.);
#3684=ORIENTED_EDGE('',*,*,#2668,.F.);
#3685=ORIENTED_EDGE('',*,*,#2669,.F.);
#3686=ORIENTED_EDGE('',*,*,#2670,.T.);
#3687=ORIENTED_EDGE('',*,*,#2671,.F.);
#3688=ORIENTED_EDGE('',*,*,#2670,.F.);
#3689=ORIENTED_EDGE('',*,*,#2672,.F.);
#3690=ORIENTED_EDGE('',*,*,#2673,.F.);
#3691=ORIENTED_EDGE('',*,*,#2674,.F.);
#3692=ORIENTED_EDGE('',*,*,#2675,.F.);
#3693=ORIENTED_EDGE('',*,*,#2676,.F.);
#3694=ORIENTED_EDGE('',*,*,#2677,.T.);
#3695=ORIENTED_EDGE('',*,*,#2678,.F.);
#3696=ORIENTED_EDGE('',*,*,#2679,.F.);
#3697=ORIENTED_EDGE('',*,*,#2680,.F.);
#3698=ORIENTED_EDGE('',*,*,#2681,.F.);
#3699=ORIENTED_EDGE('',*,*,#2682,.F.);
#3700=ORIENTED_EDGE('',*,*,#2683,.F.);
#3701=ORIENTED_EDGE('',*,*,#2677,.F.);
#3702=ORIENTED_EDGE('',*,*,#2673,.T.);
#3703=ORIENTED_EDGE('',*,*,#2684,.T.);
#3704=ORIENTED_EDGE('',*,*,#2682,.T.);
#3705=ORIENTED_EDGE('',*,*,#2685,.F.);
#3706=ORIENTED_EDGE('',*,*,#2672,.T.);
#3707=ORIENTED_EDGE('',*,*,#2686,.T.);
#3708=ORIENTED_EDGE('',*,*,#2683,.T.);
#3709=ORIENTED_EDGE('',*,*,#2684,.F.);
#3710=ORIENTED_EDGE('',*,*,#2669,.T.);
#3711=ORIENTED_EDGE('',*,*,#2687,.T.);
#3712=ORIENTED_EDGE('',*,*,#2678,.T.);
#3713=ORIENTED_EDGE('',*,*,#2686,.F.);
#3714=ORIENTED_EDGE('',*,*,#2688,.F.);
#3715=ORIENTED_EDGE('',*,*,#2689,.T.);
#3716=ORIENTED_EDGE('',*,*,#2690,.T.);
#3717=ORIENTED_EDGE('',*,*,#2689,.F.);
#3718=ORIENTED_EDGE('',*,*,#2668,.T.);
#3719=ORIENTED_EDGE('',*,*,#2691,.T.);
#3720=ORIENTED_EDGE('',*,*,#2679,.T.);
#3721=ORIENTED_EDGE('',*,*,#2687,.F.);
#3722=ORIENTED_EDGE('',*,*,#2674,.T.);
#3723=ORIENTED_EDGE('',*,*,#2685,.T.);
#3724=ORIENTED_EDGE('',*,*,#2681,.T.);
#3725=ORIENTED_EDGE('',*,*,#2692,.F.);
#3726=ORIENTED_EDGE('',*,*,#2675,.T.);
#3727=ORIENTED_EDGE('',*,*,#2692,.T.);
#3728=ORIENTED_EDGE('',*,*,#2680,.T.);
#3729=ORIENTED_EDGE('',*,*,#2691,.F.);
#3730=ORIENTED_EDGE('',*,*,#2676,.T.);
#3731=ORIENTED_EDGE('',*,*,#2688,.T.);
#3732=ORIENTED_EDGE('',*,*,#2671,.T.);
#3733=ORIENTED_EDGE('',*,*,#2690,.F.);
#3898=PLANE('',#4807);
#3899=PLANE('',#4808);
#3900=PLANE('',#4809);
#3901=PLANE('',#4813);
#3902=PLANE('',#4814);
#3903=PLANE('',#4815);
#3904=PLANE('',#4816);
#3905=PLANE('',#4817);
#4134=ADVANCED_FACE('',(#788),#215,.T.);
#4135=ADVANCED_FACE('',(#789),#216,.T.);
#4136=ADVANCED_FACE('',(#790),#3898,.T.);
#4137=ADVANCED_FACE('',(#791),#3899,.T.);
#4138=ADVANCED_FACE('',(#792),#3900,.T.);
#4139=ADVANCED_FACE('',(#793),#560,.F.);
#4140=ADVANCED_FACE('',(#794),#3901,.T.);
#4141=ADVANCED_FACE('',(#795),#3902,.T.);
#4142=ADVANCED_FACE('',(#796),#3903,.T.);
#4143=ADVANCED_FACE('',(#797,#374),#3904,.T.);
#4144=ADVANCED_FACE('',(#798,#375),#3905,.F.);
#4170=CLOSED_SHELL('',(#4134,#4135,#4136,#4137,#4138,#4139,#4140,#4141,
#4142,#4143,#4144));
#4802=AXIS2_PLACEMENT_3D('',#7188,#5994,#5995);
#4803=AXIS2_PLACEMENT_3D('',#7189,#5996,#5997);
#4804=AXIS2_PLACEMENT_3D('',#7201,#5999,#6000);
#4805=AXIS2_PLACEMENT_3D('',#7217,#6001,#6002);
#4806=AXIS2_PLACEMENT_3D('',#7219,#6003,#6004);
#4807=AXIS2_PLACEMENT_3D('',#7245,#6006,#6007);
#4808=AXIS2_PLACEMENT_3D('',#7248,#6010,#6011);
#4809=AXIS2_PLACEMENT_3D('',#7250,#6013,#6014);
#4810=AXIS2_PLACEMENT_3D('',#7252,#6016,#6017);
#4811=AXIS2_PLACEMENT_3D('',#7254,#6018,#6019);
#4812=AXIS2_PLACEMENT_3D('',#7257,#6021,#6022);
#4813=AXIS2_PLACEMENT_3D('',#7258,#6023,#6024);
#4814=AXIS2_PLACEMENT_3D('',#7260,#6026,#6027);
#4815=AXIS2_PLACEMENT_3D('',#7262,#6029,#6030);
#4816=AXIS2_PLACEMENT_3D('',#7263,#6031,#6032);
#4817=AXIS2_PLACEMENT_3D('',#7264,#6033,#6034);
#5994=DIRECTION('axis',(0.,0.,1.));
#5995=DIRECTION('refdir',(1.,0.,0.));
#5996=DIRECTION('center_axis',(0.,1.,0.));
#5997=DIRECTION('ref_axis',(1.,0.,0.));
#5998=DIRECTION('',(0.866025403784439,-0.5,1.06057523872491E-16));
#5999=DIRECTION('center_axis',(0.,-1.,0.));
#6000=DIRECTION('ref_axis',(1.,0.,0.));
#6001=DIRECTION('center_axis',(0.,-1.,0.));
#6002=DIRECTION('ref_axis',(1.,0.,0.));
#6003=DIRECTION('center_axis',(0.,1.,0.));
#6004=DIRECTION('ref_axis',(1.,0.,0.));
#6005=DIRECTION('',(-0.866025403784439,-0.5,-1.06057523872491E-16));
#6006=DIRECTION('center_axis',(1.4792020664489E-16,0.,-1.));
#6007=DIRECTION('ref_axis',(-1.,0.,-1.4792020664489E-16));
#6008=DIRECTION('',(0.,1.,0.));
#6009=DIRECTION('',(0.,1.,0.));
#6010=DIRECTION('center_axis',(-0.866025403784439,0.,-0.5));
#6011=DIRECTION('ref_axis',(-0.5,0.,0.866025403784439));
#6012=DIRECTION('',(0.,1.,0.));
#6013=DIRECTION('center_axis',(-0.866025403784439,0.,0.5));
#6014=DIRECTION('ref_axis',(0.5,0.,0.866025403784439));
#6015=DIRECTION('',(0.,1.,0.));
#6016=DIRECTION('center_axis',(0.,1.,0.));
#6017=DIRECTION('ref_axis',(1.,0.,0.));
#6018=DIRECTION('center_axis',(0.,1.,0.));
#6019=DIRECTION('ref_axis',(1.,0.,0.));
#6020=DIRECTION('',(0.,-1.,0.));
#6021=DIRECTION('center_axis',(0.,1.,0.));
#6022=DIRECTION('ref_axis',(1.,0.,0.));
#6023=DIRECTION('center_axis',(-2.95840413289779E-16,0.,1.));
#6024=DIRECTION('ref_axis',(1.,0.,2.95840413289779E-16));
#6025=DIRECTION('',(0.,1.,0.));
#6026=DIRECTION('center_axis',(0.866025403784439,0.,-0.5));
#6027=DIRECTION('ref_axis',(-0.5,0.,-0.866025403784439));
#6028=DIRECTION('',(0.,1.,0.));
#6029=DIRECTION('center_axis',(0.866025403784439,0.,0.5));
#6030=DIRECTION('ref_axis',(0.5,0.,-0.866025403784439));
#6031=DIRECTION('center_axis',(0.,1.,0.));
#6032=DIRECTION('ref_axis',(1.,0.,0.));
#6033=DIRECTION('center_axis',(0.,1.,0.));
#6034=DIRECTION('ref_axis',(1.,0.,0.));
#7188=CARTESIAN_POINT('',(0.,0.,0.));
#7189=CARTESIAN_POINT('Origin',(0.,0.067277284513851,0.));
#7190=CARTESIAN_POINT('',(-0.375277674973257,0.0768195421087395,0.65));
#7191=CARTESIAN_POINT('',(0.375277674973257,0.0768195421087395,0.65));
#7192=CARTESIAN_POINT('Ctrl Pts',(-0.375277674973257,0.0768195421087395,
0.65));
#7193=CARTESIAN_POINT('Ctrl Pts',(1.66533453693773E-13,-0.0315137912242439,
0.65));
#7194=CARTESIAN_POINT('Ctrl Pts',(0.375277674973257,0.0768195421087394,
0.65));
#7195=CARTESIAN_POINT('',(-0.750555349946514,0.0768195421087394,-9.19165206894919E-17));
#7196=CARTESIAN_POINT('Ctrl Pts',(-0.750555349946514,0.0768195421087394,
-9.19165206894919E-17));
#7197=CARTESIAN_POINT('Ctrl Pts',(-0.562916512459802,-0.0315137912242434,
0.325000000000144));
#7198=CARTESIAN_POINT('Ctrl Pts',(-0.375277674973257,0.0768195421087395,
0.65));
#7199=CARTESIAN_POINT('',(-0.6175,-2.77555756156289E-17,-7.5621939847349E-17));
#7200=CARTESIAN_POINT('',(-0.734027674973257,0.067277284513851,-8.98924642641573E-17));
#7201=CARTESIAN_POINT('Origin',(0.,0.,0.));
#7202=CARTESIAN_POINT('',(-0.375277674973257,0.0768195421087395,-0.65));
#7203=CARTESIAN_POINT('Ctrl Pts',(-0.375277674973257,0.0768195421087395,
-0.65));
#7204=CARTESIAN_POINT('Ctrl Pts',(-0.562916512459968,-0.0315137912242437,
-0.324999999999856));
#7205=CARTESIAN_POINT('Ctrl Pts',(-0.750555349946514,0.0768195421087395,
-9.19165206894919E-17));
#7206=CARTESIAN_POINT('',(0.375277674973257,0.0768195421087395,-0.65));
#7207=CARTESIAN_POINT('Ctrl Pts',(0.375277674973257,0.0768195421087395,
-0.65));
#7208=CARTESIAN_POINT('Ctrl Pts',(-1.66144875635155E-13,-0.0315137912242437,
-0.65));
#7209=CARTESIAN_POINT('Ctrl Pts',(-0.375277674973257,0.0768195421087395,
-0.65));
#7210=CARTESIAN_POINT('',(0.750555349946514,0.0768195421087394,0.));
#7211=CARTESIAN_POINT('Ctrl Pts',(0.750555349946514,0.0768195421087394,
0.));
#7212=CARTESIAN_POINT('Ctrl Pts',(0.562916512459802,-0.0315137912242436,
-0.325000000000144));
#7213=CARTESIAN_POINT('Ctrl Pts',(0.375277674973257,0.0768195421087395,
-0.65));
#7214=CARTESIAN_POINT('Ctrl Pts',(0.375277674973257,0.0768195421087394,
0.65));
#7215=CARTESIAN_POINT('Ctrl Pts',(0.562916512459968,-0.0315137912242439,
0.324999999999856));
#7216=CARTESIAN_POINT('Ctrl Pts',(0.750555349946514,0.0768195421087394,
0.));
#7217=CARTESIAN_POINT('Origin',(0.,0.612722715486149,0.));
#7218=CARTESIAN_POINT('',(-0.6175,0.68,-7.5621939847349E-17));
#7219=CARTESIAN_POINT('Origin',(0.,0.68,0.));
#7220=CARTESIAN_POINT('',(-0.750555349946514,0.603180457891261,-9.19165206894919E-17));
#7221=CARTESIAN_POINT('',(-0.734027674973257,0.612722715486149,-8.98924642641573E-17));
#7222=CARTESIAN_POINT('',(-0.375277674973257,0.603180457891261,0.65));
#7223=CARTESIAN_POINT('Ctrl Pts',(-0.375277674973257,0.603180457891261,
0.65));
#7224=CARTESIAN_POINT('Ctrl Pts',(-0.562916512459968,0.711513791224243,
0.324999999999856));
#7225=CARTESIAN_POINT('Ctrl Pts',(-0.750555349946514,0.603180457891261,
-9.19165206894919E-17));
#7226=CARTESIAN_POINT('',(0.375277674973257,0.603180457891261,0.65));
#7227=CARTESIAN_POINT('Ctrl Pts',(0.375277674973257,0.603180457891261,0.65));
#7228=CARTESIAN_POINT('Ctrl Pts',(-1.66755498298699E-13,0.711513791224244,
0.65));
#7229=CARTESIAN_POINT('Ctrl Pts',(-0.375277674973257,0.603180457891261,
0.65));
#7230=CARTESIAN_POINT('',(0.750555349946514,0.603180457891261,0.));
#7231=CARTESIAN_POINT('Ctrl Pts',(0.750555349946514,0.603180457891261,0.));
#7232=CARTESIAN_POINT('Ctrl Pts',(0.562916512459802,0.711513791224244,0.325000000000144));
#7233=CARTESIAN_POINT('Ctrl Pts',(0.375277674973257,0.603180457891261,0.65));
#7234=CARTESIAN_POINT('',(0.375277674973257,0.603180457891261,-0.65));
#7235=CARTESIAN_POINT('Ctrl Pts',(0.375277674973257,0.603180457891261,-0.65));
#7236=CARTESIAN_POINT('Ctrl Pts',(0.562916512459969,0.711513791224244,-0.324999999999856));
#7237=CARTESIAN_POINT('Ctrl Pts',(0.750555349946514,0.603180457891261,0.));
#7238=CARTESIAN_POINT('',(-0.375277674973257,0.603180457891261,-0.65));
#7239=CARTESIAN_POINT('Ctrl Pts',(-0.375277674973257,0.603180457891261,
-0.65));
#7240=CARTESIAN_POINT('Ctrl Pts',(1.66422431391311E-13,0.711513791224244,
-0.65));
#7241=CARTESIAN_POINT('Ctrl Pts',(0.375277674973257,0.603180457891261,-0.65));
#7242=CARTESIAN_POINT('Ctrl Pts',(-0.750555349946514,0.603180457891261,
-9.19165206894919E-17));
#7243=CARTESIAN_POINT('Ctrl Pts',(-0.562916512459802,0.711513791224244,
-0.325000000000144));
#7244=CARTESIAN_POINT('Ctrl Pts',(-0.375277674973257,0.603180457891261,
-0.65));
#7245=CARTESIAN_POINT('Origin',(0.375277674973257,0.,-0.65));
#7246=CARTESIAN_POINT('',(-0.375277674973257,0.,-0.65));
#7247=CARTESIAN_POINT('',(0.375277674973257,0.,-0.65));
#7248=CARTESIAN_POINT('Origin',(-0.375277674973257,0.,-0.65));
#7249=CARTESIAN_POINT('',(-0.750555349946514,0.,-9.19165206894919E-17));
#7250=CARTESIAN_POINT('Origin',(-0.750555349946514,0.,-9.19165206894919E-17));
#7251=CARTESIAN_POINT('',(-0.375277674973257,0.,0.65));
#7252=CARTESIAN_POINT('Origin',(0.,0.,0.));
#7253=CARTESIAN_POINT('',(-0.338975,0.68,4.15124648740974E-17));
#7254=CARTESIAN_POINT('Origin',(0.,0.68,0.));
#7255=CARTESIAN_POINT('',(-0.338975,0.,4.15124648740974E-17));
#7256=CARTESIAN_POINT('',(-0.338975,0.,4.15124648740974E-17));
#7257=CARTESIAN_POINT('Origin',(0.,0.,0.));
#7258=CARTESIAN_POINT('Origin',(-0.375277674973257,0.,0.65));
#7259=CARTESIAN_POINT('',(0.375277674973257,0.,0.65));
#7260=CARTESIAN_POINT('Origin',(0.750555349946514,0.,0.));
#7261=CARTESIAN_POINT('',(0.750555349946514,0.,0.));
#7262=CARTESIAN_POINT('Origin',(0.375277674973257,0.,0.65));
#7263=CARTESIAN_POINT('Origin',(0.,0.68,-1.11022302462516E-16));
#7264=CARTESIAN_POINT('Origin',(0.,0.,-1.11022302462516E-16));
#7315=UNCERTAINTY_MEASURE_WITH_UNIT(LENGTH_MEASURE(0.001),#7345,
'DISTANCE_ACCURACY_VALUE',
'Maximum model space distance between geometric entities at asserted c
onnectivities');
#7318=UNCERTAINTY_MEASURE_WITH_UNIT(LENGTH_MEASURE(0.001),#7345,
'DISTANCE_ACCURACY_VALUE',
'Maximum model space distance between geometric entities at asserted c
onnectivities');
#7341=(
GEOMETRIC_REPRESENTATION_CONTEXT(3)
GLOBAL_UNCERTAINTY_ASSIGNED_CONTEXT((#7315))
GLOBAL_UNIT_ASSIGNED_CONTEXT((#7345,#7347,#7348))
REPRESENTATION_CONTEXT('','3D')
);
#7344=(
GEOMETRIC_REPRESENTATION_CONTEXT(3)
GLOBAL_UNCERTAINTY_ASSIGNED_CONTEXT((#7318))
GLOBAL_UNIT_ASSIGNED_CONTEXT((#7345,#7347,#7348))
REPRESENTATION_CONTEXT('','3D')
);
#7345=(
LENGTH_UNIT()
NAMED_UNIT(*)
SI_UNIT(.CENTI.,.METRE.)
);
#7347=(
NAMED_UNIT(*)
PLANE_ANGLE_UNIT()
SI_UNIT($,.RADIAN.)
);
#7348=(
NAMED_UNIT(*)
SI_UNIT($,.STERADIAN.)
SOLID_ANGLE_UNIT()
);
#7371=SHAPE_DEFINITION_REPRESENTATION(#7419,#7462);
#7419=PRODUCT_DEFINITION_SHAPE('',$,#7488);
#7462=SHAPE_REPRESENTATION('',(#4802),#7341);
#7465=PRODUCT_DEFINITION_CONTEXT('part definition',#7542,'design');
#7488=PRODUCT_DEFINITION('Hex Nut - M8','Hex Nut - M8',#7513,#7465);
#7513=PRODUCT_DEFINITION_FORMATION('',$,#7566);
#7542=APPLICATION_CONTEXT(
'Core Data for Automotive Mechanical Design Process');
#7543=PRODUCT_CONTEXT('part definition',#7542,'mechanical');
#7566=PRODUCT('Hex Nut - M8','Hex Nut - M8','Hex Nut - M8',(#7543));
#7632=COLOUR_RGB('Black',0.12,0.14,0.17);
#7633=FILL_AREA_STYLE_COLOUR('',#7632);
#7634=FILL_AREA_STYLE('',(#7633));
#7635=SURFACE_STYLE_FILL_AREA(#7634);
#7636=SURFACE_SIDE_STYLE('',(#7635));
#7637=SURFACE_STYLE_USAGE(.BOTH.,#7636);
#7638=PRESENTATION_STYLE_ASSIGNMENT((#7637));
ENDSEC;
END-ISO-10303-21;
